ISO-10303-21;
HEADER;
FILE_DESCRIPTION (('STEP AP214'),
    '1' );
FILE_NAME ('small revit.step',
    '2026-10-28T16:30:29',
    ( '' ),
    ( '' ),
    'SwSTEP 2.0',
    'SolidWorks 2025',
    '' );
FILE_SCHEMA (( 'AUTOMOTIVE_DESIGN' ));
ENDSEC;

DATA;
#29=CARTESIAN_POINT ( 'NONE',  ( 30.00000000000000000, 0.000000000000000000, 0.000000000000000000 ) ) ;
#56=ORIENTED_EDGE ( 'NONE', *, *, #1998, .T. ) ;
#58=CONICAL_SURFACE ( 'NONE', #5587, 8.000000000000003553, 0.7853981633974447263 ) ;
#59=CARTESIAN_POINT ( 'NONE',  ( 30.00000000000000000, 0.000000000000000000, 0.000000000000000000 ) ) ;
#62=DIRECTION ( 'NONE',  ( 0.000000000000000000, 0.000000000000000000, 1.000000000000000000 ) ) ;
#108=CARTESIAN_POINT ( 'NONE',  ( 0.000000000000000000, 0.000000000000000000, 0.000000000000000000 ) ) ;
#128=AXIS2_PLACEMENT_3D ( 'NONE', #2301, #7483, #6908 ) ;
#157=PLANE ( 'NONE',  #5099 ) ;
#195=DIRECTION ( 'NONE',  ( 1.000000000000000000, 2.624548829666596736E-30, -9.231085635203017994E-31 ) ) ;
#216=CARTESIAN_POINT ( 'NONE',  ( 26.00000000000000000, 0.000000000000000000, 6.000000000000003553 ) ) ;
#218=EDGE_LOOP ( 'NONE', ( #4919, #3639 ) ) ;
#245=VERTEX_POINT ( 'NONE', #3715 ) ;
#253=FACE_OUTER_BOUND ( 'NONE', #6708, .T. ) ;
#269=ORIENTED_EDGE ( 'NONE', *, *, #1198, .F. ) ;
#286=ADVANCED_FACE ( 'NONE', ( #6562 ), #7173, .F. ) ;
#307=EDGE_CURVE ( 'NONE', #2650, #6611, #1827, .T. ) ;
#314=( GEOMETRIC_REPRESENTATION_CONTEXT ( 3 ) GLOBAL_UNCERTAINTY_ASSIGNED_CONTEXT ( ( #560 ) ) GLOBAL_UNIT_ASSIGNED_CONTEXT ( ( #5090, #1047, #4439 ) ) REPRESENTATION_CONTEXT ( 'NONE', 'WORKASPACE' ) );
#350=DIRECTION ( 'NONE',  ( -1.000000000000000000, -2.624548829666596736E-30, 9.231085635203017994E-31 ) ) ;
#366=PLANE ( 'NONE',  #3453 ) ;
#417=CIRCLE ( 'NONE', #4735, 10.00000000000000355 ) ;
#454=CARTESIAN_POINT ( 'NONE',  ( 30.00000000000000000, 0.000000000000000000, 0.000000000000000000 ) ) ;
#456=CARTESIAN_POINT ( 'NONE',  ( 30.00000000000000000, 1.224646799147353651E-15, -10.00000000000000355 ) ) ;
#539=VECTOR ( 'NONE', #7469, 1000.000000000000000 ) ;
#552=VECTOR ( 'NONE', #4432, 1000.000000000000114 ) ;
#560=UNCERTAINTY_MEASURE_WITH_UNIT (LENGTH_MEASURE( 1.000000000000000082E-05 ), #5090, 'distance_accuracy_value', 'NONE');
#573=AXIS2_PLACEMENT_3D ( 'NONE', #6167, #1981, #896 ) ;
#608=CARTESIAN_POINT ( 'NONE',  ( 4.000000000000000000, 0.000000000000000000, 0.000000000000000000 ) ) ;
#620=AXIS2_PLACEMENT_3D ( 'NONE', #29, #3539, #7112 ) ;
#629=CIRCLE ( 'NONE', #6648, 6.000000000000003553 ) ;
#668=DIRECTION ( 'NONE',  ( 9.231085635203014490E-31, 0.000000000000000000, -1.000000000000000000 ) ) ;
#690=DIRECTION ( 'NONE',  ( 9.231085635203014490E-31, 0.000000000000000000, -1.000000000000000000 ) ) ;
#702=EDGE_CURVE ( 'NONE', #3466, #1233, #6402, .T. ) ;
#748=EDGE_CURVE ( 'NONE', #3851, #245, #1979, .T. ) ;
#757=EDGE_CURVE ( 'NONE', #2650, #2663, #6890, .T. ) ;
#765=ORIENTED_EDGE ( 'NONE', *, *, #757, .F. ) ;
#775=CARTESIAN_POINT ( 'NONE',  ( 27.99999999999998579, 1.224646799147344973E-15, -9.999999999999998224 ) ) ;
#784=ORIENTED_EDGE ( 'NONE', *, *, #962, .F. ) ;
#811=DIRECTION ( 'NONE',  ( 0.000000000000000000, 0.000000000000000000, -1.000000000000000000 ) ) ;
#848=CARTESIAN_POINT ( 'NONE',  ( 0.000000000000000000, 0.000000000000000000, 0.000000000000000000 ) ) ;
#855=CIRCLE ( 'NONE', #6519, 10.00000000000000355 ) ;
#878=CIRCLE ( 'NONE', #3472, 10.00000000000000355 ) ;
#888=ORIENTED_EDGE ( 'NONE', *, *, #1938, .F. ) ;
#896=DIRECTION ( 'NONE',  ( 0.000000000000000000, 0.000000000000000000, 1.000000000000000000 ) ) ;
#907=ORIENTED_EDGE ( 'NONE', *, *, #2968, .T. ) ;
#924=CARTESIAN_POINT ( 'NONE',  ( 7.384868508162405987E-30, 0.000000000000000000, -7.999999999999992895 ) ) ;
#958=DIRECTION ( 'NONE',  ( 0.000000000000000000, 0.000000000000000000, 1.000000000000000000 ) ) ;
#959=VERTEX_POINT ( 'NONE', #924 ) ;
#962=EDGE_CURVE ( 'NONE', #2663, #2650, #629, .T. ) ;
#987=ORIENTED_EDGE ( 'NONE', *, *, #4853, .T. ) ;
#1041=AXIS2_PLACEMENT_3D ( 'NONE', #3695, #6142, #6073 ) ;
#1047=( NAMED_UNIT ( * ) PLANE_ANGLE_UNIT ( ) SI_UNIT ( $, .RADIAN. ) );
#1069=CIRCLE ( 'NONE', #2422, 10.00000000000000355 ) ;
#1181=CYLINDRICAL_SURFACE ( 'NONE', #620, 10.00000000000000355 ) ;
#1191=ORIENTED_EDGE ( 'NONE', *, *, #748, .F. ) ;
#1192=AXIS2_PLACEMENT_3D ( 'NONE', #848, #2553, #6193 ) ;
#1196=ORIENTED_EDGE ( 'NONE', *, *, #5482, .T. ) ;
#1198=EDGE_CURVE ( 'NONE', #7257, #1233, #3549, .T. ) ;
#1206=SHAPE_REPRESENTATION ( 'small revit', ( #1914 ), #314 ) ;
#1219=FACE_OUTER_BOUND ( 'NONE', #2393, .T. ) ;
#1226=VERTEX_POINT ( 'NONE', #6115 ) ;
#1233=VERTEX_POINT ( 'NONE', #2608 ) ;
#1239=CARTESIAN_POINT ( 'NONE',  ( 26.00000000000000000, 0.000000000000000000, 0.000000000000000000 ) ) ;
#1245=LINE ( 'NONE', #3025, #5956 ) ;
#1296=CARTESIAN_POINT ( 'NONE',  ( 27.99999999999998579, -7.873646488999802468E-30, 9.999999999999998224 ) ) ;
#1320=DIRECTION ( 'NONE',  ( 1.000000000000000000, 2.624548829666596385E-30, 9.231085635203014490E-31 ) ) ;
#1323=FACE_OUTER_BOUND ( 'NONE', #6585, .T. ) ;
#1357=DIRECTION ( 'NONE',  ( 0.000000000000000000, 0.000000000000000000, -1.000000000000000000 ) ) ;
#1420=EDGE_LOOP ( 'NONE', ( #7359, #3970 ) ) ;
#1508=AXIS2_PLACEMENT_3D ( 'NONE', #5142, #6249, #3374 ) ;
#1530=ADVANCED_FACE ( 'NONE', ( #2635 ), #3834, .T. ) ;
#1531=CARTESIAN_POINT ( 'NONE',  ( 30.00000000000000000, 0.000000000000000000, 0.000000000000000000 ) ) ;
#1536=ORIENTED_EDGE ( 'NONE', *, *, #5988, .F. ) ;
#1555=DIRECTION ( 'NONE',  ( 1.000000000000000000, 2.624548829666596385E-30, 9.231085635203014490E-31 ) ) ;
#1558=ORIENTED_EDGE ( 'NONE', *, *, #6596, .T. ) ;
#1567=EDGE_LOOP ( 'NONE', ( #5763, #3668 ) ) ;
#1572=VERTEX_POINT ( 'NONE', #6334 ) ;
#1620=CARTESIAN_POINT ( 'NONE',  ( 4.000000000000000000, 0.000000000000000000, 10.00000000000000355 ) ) ;
#1666=CARTESIAN_POINT ( 'NONE',  ( 27.99999999999998579, 0.000000000000000000, 0.000000000000000000 ) ) ;
#1705=ORIENTED_EDGE ( 'NONE', *, *, #3108, .T. ) ;
#1714=AXIS2_PLACEMENT_3D ( 'NONE', #1666, #4558, #2784 ) ;
#1722=ORIENTED_EDGE ( 'NONE', *, *, #307, .T. ) ;
#1733=ORIENTED_EDGE ( 'NONE', *, *, #3849, .T. ) ;
#1744=PRODUCT_DEFINITION ( 'UNKNOWN', '', #2154, #3229 ) ;
#1749=CARTESIAN_POINT ( 'NONE',  ( 0.000000000000000000, 0.000000000000000000, 0.000000000000000000 ) ) ;
#1761=ADVANCED_FACE ( 'NONE', ( #1824, #1896 ), #5938, .F. ) ;
#1824=FACE_BOUND ( 'NONE', #5461, .T. ) ;
#1827=LINE ( 'NONE', #216, #1842 ) ;
#1842=VECTOR ( 'NONE', #1867, 1000.000000000000000 ) ;
#1857=DIRECTION ( 'NONE',  ( 1.000000000000000000, 2.624548829666596736E-30, -9.231085635203017994E-31 ) ) ;
#1864=DIRECTION ( 'NONE',  ( 1.000000000000000000, 0.000000000000000000, 0.000000000000000000 ) ) ;
#1867=DIRECTION ( 'NONE',  ( -1.000000000000000000, -2.624548829666596736E-30, 9.231085635203017994E-31 ) ) ;
#1896=FACE_OUTER_BOUND ( 'NONE', #1567, .T. ) ;
#1911=CARTESIAN_POINT ( 'NONE',  ( 2.000000000000001776, 0.000000000000000000, 0.000000000000000000 ) ) ;
#1914=AXIS2_PLACEMENT_3D ( 'NONE', #1749, #62, #1864 ) ;
#1936=VERTEX_POINT ( 'NONE', #775 ) ;
#1938=EDGE_CURVE ( 'NONE', #959, #4660, #7098, .T. ) ;
#1976=DIRECTION ( 'NONE',  ( 1.000000000000000000, 2.624548829666596385E-30, 9.231085635203014490E-31 ) ) ;
#1979=CIRCLE ( 'NONE', #6765, 10.00000000000000355 ) ;
#1981=DIRECTION ( 'NONE',  ( -1.000000000000000000, -2.624548829666596736E-30, 9.231085635203017994E-31 ) ) ;
#1998=EDGE_CURVE ( 'NONE', #1936, #7257, #1069, .T. ) ;
#2008=CIRCLE ( 'NONE', #1508, 6.000000000000003553 ) ;
#2087=CYLINDRICAL_SURFACE ( 'NONE', #3872, 6.000000000000003553 ) ;
#2090=CLOSED_SHELL ( 'NONE', ( #2904, #4938, #3218, #6795, #1530, #5222, #5447, #286, #2729, #7031, #3531, #1761, #6303, #5149 ) ) ;
#2108=CARTESIAN_POINT ( 'NONE',  ( 26.00000000000000000, 0.000000000000000000, 0.000000000000000000 ) ) ;
#2136=DIRECTION ( 'NONE',  ( 9.231085635203014490E-31, 0.000000000000000000, -1.000000000000000000 ) ) ;
#2149=AXIS2_PLACEMENT_3D ( 'NONE', #59, #7020, #6486 ) ;
#2154=PRODUCT_DEFINITION_FORMATION_WITH_SPECIFIED_SOURCE ( 'ANY', '', #2227, .NOT_KNOWN. ) ;
#2202=CARTESIAN_POINT ( 'NONE',  ( 26.00000000000000000, 0.000000000000000000, 0.000000000000000000 ) ) ;
#2222=AXIS2_PLACEMENT_3D ( 'NONE', #1239, #3708, #5975 ) ;
#2227=PRODUCT ( 'small revit', 'small revit', '', ( #6516 ) ) ;
#2243=AXIS2_PLACEMENT_3D ( 'NONE', #7213, #4908, #5407 ) ;
#2244=ORIENTED_EDGE ( 'NONE', *, *, #6586, .F. ) ;
#2271=MECHANICAL_DESIGN_GEOMETRIC_PRESENTATION_REPRESENTATION('',(#5582),#3865);
#2301=CARTESIAN_POINT ( 'NONE',  ( 4.000000000000000000, 0.000000000000000000, 0.000000000000000000 ) ) ;
#2310=EDGE_LOOP ( 'NONE', ( #2244, #6766, #4084, #7389 ) ) ;
#2322=SHAPE_DEFINITION_REPRESENTATION ( #7500, #1206 ) ;
#2328=DIRECTION ( 'NONE',  ( -0.7071067811865497932, -1.855836275012473479E-30, 0.7071067811865452413 ) ) ;
#2350=AXIS2_PLACEMENT_3D ( 'NONE', #3057, #5401, #6480 ) ;
#2371=EDGE_LOOP ( 'NONE', ( #3580, #1196, #6171, #5089 ) ) ;
#2393=EDGE_LOOP ( 'NONE', ( #1733, #1705, #3392, #269 ) ) ;
#2396=CIRCLE ( 'NONE', #2149, 8.000000000000003553 ) ;
#2422=AXIS2_PLACEMENT_3D ( 'NONE', #6996, #2957, #5884 ) ;
#2426=DIRECTION ( 'NONE',  ( -1.000000000000000000, -2.624548829666596736E-30, 9.231085635203017994E-31 ) ) ;
#2517=AXIS2_PLACEMENT_3D ( 'NONE', #6904, #3986, #4565 ) ;
#2553=DIRECTION ( 'NONE',  ( -1.000000000000000000, -2.624548829666596736E-30, 9.231085635203017994E-31 ) ) ;
#2555=APPLICATION_CONTEXT ( 'automotive_design' ) ;
#2608=CARTESIAN_POINT ( 'NONE',  ( 26.00000000000000000, -7.873646488999802468E-30, 9.999999999999998224 ) ) ;
#2635=FACE_OUTER_BOUND ( 'NONE', #2371, .T. ) ;
#2646=ORIENTED_EDGE ( 'NONE', *, *, #3787, .T. ) ;
#2650=VERTEX_POINT ( 'NONE', #3837 ) ;
#2663=VERTEX_POINT ( 'NONE', #5636 ) ;
#2670=ORIENTED_EDGE ( 'NONE', *, *, #5988, .T. ) ;
#2729=ADVANCED_FACE ( 'NONE', ( #1323 ), #3758, .T. ) ;
#2760=CIRCLE ( 'NONE', #5221, 7.999999999999992895 ) ;
#2784=DIRECTION ( 'NONE',  ( 0.000000000000000000, 0.000000000000000000, -1.000000000000000000 ) ) ;
#2803=LINE ( 'NONE', #456, #3843 ) ;
#2816=SHAPE_REPRESENTATION_RELATIONSHIP ( 'NONE' , 'NONE' ,  #1206, #4093 ) ;
#2874=DIRECTION ( 'NONE',  ( 0.000000000000000000, 0.000000000000000000, 1.000000000000000000 ) ) ;
#2881=VECTOR ( 'NONE', #4703, 1000.000000000000000 ) ;
#2886=EDGE_LOOP ( 'NONE', ( #1536, #5079 ) ) ;
#2904=ADVANCED_FACE ( 'NONE', ( #5037 ), #6286, .T. ) ;
#2948=( NAMED_UNIT ( * ) PLANE_ANGLE_UNIT ( ) SI_UNIT ( $, .RADIAN. ) );
#2957=DIRECTION ( 'NONE',  ( -1.000000000000000000, -2.624548829666596736E-30, 9.231085635203017994E-31 ) ) ;
#2968=EDGE_CURVE ( 'NONE', #1233, #3466, #878, .T. ) ;
#3025=CARTESIAN_POINT ( 'NONE',  ( 2.000000000000001776, 0.000000000000000000, -10.00000000000000355 ) ) ;
#3057=CARTESIAN_POINT ( 'NONE',  ( 26.00000000000000000, 0.000000000000000000, 0.000000000000000000 ) ) ;
#3082=CARTESIAN_POINT ( 'NONE',  ( 30.00000000000000000, 0.000000000000000000, 10.00000000000000355 ) ) ;
#3108=EDGE_CURVE ( 'NONE', #1936, #3466, #2803, .T. ) ;
#3140=DIRECTION ( 'NONE',  ( 1.000000000000000000, 2.624548829666596385E-30, 9.231085635203014490E-31 ) ) ;
#3152=DIRECTION ( 'NONE',  ( 0.000000000000000000, 0.000000000000000000, 1.000000000000000000 ) ) ;
#3173=DIRECTION ( 'NONE',  ( 1.000000000000000000, 2.624548829666596736E-30, -9.231085635203017994E-31 ) ) ;
#3187=DIRECTION ( 'NONE',  ( -1.000000000000000000, -2.624548829666596736E-30, 9.231085635203017994E-31 ) ) ;
#3218=ADVANCED_FACE ( 'NONE', ( #1219 ), #1181, .T. ) ;
#3228=DIRECTION ( 'NONE',  ( 1.000000000000000000, 2.624548829666596736E-30, -9.231085635203017994E-31 ) ) ;
#3229=PRODUCT_DEFINITION_CONTEXT ( 'detailed design', #2555, 'design' ) ;
#3237=LINE ( 'NONE', #5586, #552 ) ;
#3277=DIRECTION ( 'NONE',  ( 1.000000000000000000, 2.624548829666596736E-30, -9.231085635203017994E-31 ) ) ;
#3300=ORIENTED_EDGE ( 'NONE', *, *, #3787, .F. ) ;
#3354=DIRECTION ( 'NONE',  ( 0.000000000000000000, 0.000000000000000000, 1.000000000000000000 ) ) ;
#3355=EDGE_LOOP ( 'NONE', ( #784, #987, #5308, #7418 ) ) ;
#3359=CARTESIAN_POINT ( 'NONE',  ( 26.00000000000000000, 7.347880794884123680E-16, -6.000000000000003553 ) ) ;
#3366=ORIENTED_EDGE ( 'NONE', *, *, #4384, .T. ) ;
#3374=DIRECTION ( 'NONE',  ( 0.000000000000000000, 0.000000000000000000, -1.000000000000000000 ) ) ;
#3392=ORIENTED_EDGE ( 'NONE', *, *, #702, .T. ) ;
#3453=AXIS2_PLACEMENT_3D ( 'NONE', #7402, #1555, #2136 ) ;
#3466=VERTEX_POINT ( 'NONE', #5108 ) ;
#3472=AXIS2_PLACEMENT_3D ( 'NONE', #2108, #3228, #4963 ) ;
#3505=VECTOR ( 'NONE', #2328, 1000.000000000000227 ) ;
#3514=EDGE_CURVE ( 'NONE', #1226, #1572, #4679, .T. ) ;
#3531=ADVANCED_FACE ( 'NONE', ( #7447 ), #366, .T. ) ;
#3539=DIRECTION ( 'NONE',  ( -1.000000000000000000, -2.624548829666596736E-30, 9.231085635203017994E-31 ) ) ;
#3549=LINE ( 'NONE', #3082, #7504 ) ;
#3554=DIRECTION ( 'NONE',  ( 1.000000000000000000, 2.624548829666596736E-30, -9.231085635203017994E-31 ) ) ;
#3562=CARTESIAN_POINT ( 'NONE',  ( 0.000000000000000000, 0.000000000000000000, 0.000000000000000000 ) ) ;
#3579=VERTEX_POINT ( 'NONE', #6490 ) ;
#3580=ORIENTED_EDGE ( 'NONE', *, *, #3514, .F. ) ;
#3639=ORIENTED_EDGE ( 'NONE', *, *, #3514, .T. ) ;
#3668=ORIENTED_EDGE ( 'NONE', *, *, #702, .F. ) ;
#3670=FACE_OUTER_BOUND ( 'NONE', #6296, .T. ) ;
#3695=CARTESIAN_POINT ( 'NONE',  ( 30.00000000000000000, 0.000000000000000000, 0.000000000000000000 ) ) ;
#3708=DIRECTION ( 'NONE',  ( 1.000000000000000000, 2.624548829666596736E-30, -9.231085635203017994E-31 ) ) ;
#3715=CARTESIAN_POINT ( 'NONE',  ( 2.000000000000001776, -2.624548829666593232E-30, 9.999999999999998224 ) ) ;
#3758=CYLINDRICAL_SURFACE ( 'NONE', #2243, 6.000000000000003553 ) ;
#3786=ORIENTED_EDGE ( 'NONE', *, *, #6522, .F. ) ;
#3787=EDGE_CURVE ( 'NONE', #245, #3851, #855, .T. ) ;
#3795=ORIENTED_EDGE ( 'NONE', *, *, #1198, .T. ) ;
#3834=CYLINDRICAL_SURFACE ( 'NONE', #573, 10.00000000000000355 ) ;
#3837=CARTESIAN_POINT ( 'NONE',  ( 26.00000000000000000, -2.887003712633254693E-29, 6.000000000000000888 ) ) ;
#3843=VECTOR ( 'NONE', #5806, 1000.000000000000000 ) ;
#3849=EDGE_CURVE ( 'NONE', #7257, #1936, #5039, .T. ) ;
#3851=VERTEX_POINT ( 'NONE', #4023 ) ;
#3865=( GEOMETRIC_REPRESENTATION_CONTEXT ( 3 ) GLOBAL_UNCERTAINTY_ASSIGNED_CONTEXT ( ( #5185 ) ) GLOBAL_UNIT_ASSIGNED_CONTEXT ( ( #4108, #2948, #4412 ) ) REPRESENTATION_CONTEXT ( 'NONE', 'WORKASPACE' ) );
#3872=AXIS2_PLACEMENT_3D ( 'NONE', #2202, #350, #6196 ) ;
#3893=EDGE_CURVE ( 'NONE', #1572, #245, #4481, .T. ) ;
#3917=CARTESIAN_POINT ( 'NONE',  ( 30.00000000000000000, -2.624548829666611800E-30, 8.000000000000000000 ) ) ;
#3970=ORIENTED_EDGE ( 'NONE', *, *, #6522, .T. ) ;
#3986=DIRECTION ( 'NONE',  ( 1.000000000000000000, 2.624548829666596736E-30, -9.231085635203017994E-31 ) ) ;
#4023=CARTESIAN_POINT ( 'NONE',  ( 2.000000000000001776, 1.224646799147350101E-15, -9.999999999999998224 ) ) ;
#4084=ORIENTED_EDGE ( 'NONE', *, *, #3849, .F. ) ;
#4093=ADVANCED_BREP_SHAPE_REPRESENTATION ( '', ( #6277, #1914 ), #314 ) ;
#4100=CARTESIAN_POINT ( 'NONE',  ( 30.00000000000000000, 0.000000000000000000, 8.000000000000003553 ) ) ;
#4108=( LENGTH_UNIT ( ) NAMED_UNIT ( * ) SI_UNIT ( .MILLI., .METRE. ) );
#4113=CONICAL_SURFACE ( 'NONE', #5083, 10.00000000000000355, 0.7853981633974500554 ) ;
#4116=ORIENTED_EDGE ( 'NONE', *, *, #5624, .F. ) ;
#4163=LINE ( 'NONE', #5853, #2881 ) ;
#4255=CARTESIAN_POINT ( 'NONE',  ( 26.00000000000000000, 0.000000000000000000, 0.000000000000000000 ) ) ;
#4289=CARTESIAN_POINT ( 'NONE',  ( 4.000000000000000000, -2.887003712633254693E-29, 6.000000000000000888 ) ) ;
#4316=FACE_OUTER_BOUND ( 'NONE', #4946, .T. ) ;
#4384=EDGE_CURVE ( 'NONE', #4660, #245, #3237, .T. ) ;
#4412=( NAMED_UNIT ( * ) SI_UNIT ( $, .STERADIAN. ) SOLID_ANGLE_UNIT ( ) );
#4432=DIRECTION ( 'NONE',  ( 0.7071067811865461294, 8.659560562355135004E-17, 0.7071067811865489050 ) ) ;
#4439=( NAMED_UNIT ( * ) SI_UNIT ( $, .STERADIAN. ) SOLID_ANGLE_UNIT ( ) );
#4445=ORIENTED_EDGE ( 'NONE', *, *, #3108, .F. ) ;
#4481=LINE ( 'NONE', #1620, #6674 ) ;
#4558=DIRECTION ( 'NONE',  ( -1.000000000000000000, -2.624548829666596736E-30, 9.231085635203017994E-31 ) ) ;
#4565=DIRECTION ( 'NONE',  ( 0.000000000000000000, 0.000000000000000000, -1.000000000000000000 ) ) ;
#4572=ORIENTED_EDGE ( 'NONE', *, *, #6586, .T. ) ;
#4584=DIRECTION ( 'NONE',  ( -1.000000000000000000, -2.624548829666596736E-30, 9.231085635203017994E-31 ) ) ;
#4611=CIRCLE ( 'NONE', #2517, 6.000000000000003553 ) ;
#4618=FACE_OUTER_BOUND ( 'NONE', #5726, .T. ) ;
#4630=VERTEX_POINT ( 'NONE', #3917 ) ;
#4648=DIRECTION ( 'NONE',  ( 0.7071067811865461294, 1.855836275012464020E-30, -0.7071067811865489050 ) ) ;
#4660=VERTEX_POINT ( 'NONE', #6236 ) ;
#4679=CIRCLE ( 'NONE', #128, 10.00000000000000355 ) ;
#4703=DIRECTION ( 'NONE',  ( -1.000000000000000000, -2.624548829666596736E-30, 9.231085635203017994E-31 ) ) ;
#4712=ORIENTED_EDGE ( 'NONE', *, *, #4384, .F. ) ;
#4735=AXIS2_PLACEMENT_3D ( 'NONE', #4924, #195, #5007 ) ;
#4824=DIRECTION ( 'NONE',  ( 0.000000000000000000, 0.000000000000000000, -1.000000000000000000 ) ) ;
#4841=DIRECTION ( 'NONE',  ( 1.000000000000000000, 2.624548829666596736E-30, -9.231085635203017994E-31 ) ) ;
#4853=EDGE_CURVE ( 'NONE', #2663, #3579, #5128, .T. ) ;
#4889=AXIS2_PLACEMENT_3D ( 'NONE', #4255, #1320, #668 ) ;
#4908=DIRECTION ( 'NONE',  ( -1.000000000000000000, -2.624548829666596736E-30, 9.231085635203017994E-31 ) ) ;
#4919=ORIENTED_EDGE ( 'NONE', *, *, #5550, .T. ) ;
#4924=CARTESIAN_POINT ( 'NONE',  ( 4.000000000000000000, 0.000000000000000000, 0.000000000000000000 ) ) ;
#4938=ADVANCED_FACE ( 'NONE', ( #3670 ), #4113, .T. ) ;
#4946=EDGE_LOOP ( 'NONE', ( #6013, #4116, #5958, #5618 ) ) ;
#4963=DIRECTION ( 'NONE',  ( 0.000000000000000000, 0.000000000000000000, -1.000000000000000000 ) ) ;
#5007=DIRECTION ( 'NONE',  ( 0.000000000000000000, 0.000000000000000000, -1.000000000000000000 ) ) ;
#5037=FACE_OUTER_BOUND ( 'NONE', #2310, .T. ) ;
#5039=CIRCLE ( 'NONE', #1714, 10.00000000000000355 ) ;
#5069=ORIENTED_EDGE ( 'NONE', *, *, #6596, .F. ) ;
#5079=ORIENTED_EDGE ( 'NONE', *, *, #6363, .F. ) ;
#5083=AXIS2_PLACEMENT_3D ( 'NONE', #7089, #3554, #4824 ) ;
#5088=FACE_OUTER_BOUND ( 'NONE', #3355, .T. ) ;
#5089=ORIENTED_EDGE ( 'NONE', *, *, #3893, .F. ) ;
#5090=( LENGTH_UNIT ( ) NAMED_UNIT ( * ) SI_UNIT ( .MILLI., .METRE. ) );
#5099=AXIS2_PLACEMENT_3D ( 'NONE', #608, #3140, #690 ) ;
#5108=CARTESIAN_POINT ( 'NONE',  ( 26.00000000000000000, 1.224646799147344973E-15, -9.999999999999998224 ) ) ;
#5128=LINE ( 'NONE', #3359, #539 ) ;
#5142=CARTESIAN_POINT ( 'NONE',  ( 4.000000000000000000, 0.000000000000000000, 0.000000000000000000 ) ) ;
#5149=ADVANCED_FACE ( 'NONE', ( #4316 ), #58, .T. ) ;
#5161=AXIS2_PLACEMENT_3D ( 'NONE', #108, #1976, #5375 ) ;
#5185=UNCERTAINTY_MEASURE_WITH_UNIT (LENGTH_MEASURE( 1.000000000000000082E-05 ), #4108, 'distance_accuracy_value', 'NONE');
#5221=AXIS2_PLACEMENT_3D ( 'NONE', #3562, #5833, #7591 ) ;
#5222=ADVANCED_FACE ( 'NONE', ( #6924 ), #5694, .T. ) ;
#5227=CYLINDRICAL_SURFACE ( 'NONE', #6807, 10.00000000000000355 ) ;
#5273=FACE_BOUND ( 'NONE', #2886, .T. ) ;
#5308=ORIENTED_EDGE ( 'NONE', *, *, #6363, .T. ) ;
#5375=DIRECTION ( 'NONE',  ( 9.231085635203014490E-31, 0.000000000000000000, -1.000000000000000000 ) ) ;
#5401=DIRECTION ( 'NONE',  ( 1.000000000000000000, 2.624548829666596736E-30, -9.231085635203017994E-31 ) ) ;
#5407=DIRECTION ( 'NONE',  ( 0.000000000000000000, 0.000000000000000000, 1.000000000000000000 ) ) ;
#5447=ADVANCED_FACE ( 'NONE', ( #5273, #5963 ), #157, .T. ) ;
#5461=EDGE_LOOP ( 'NONE', ( #6578, #5644 ) ) ;
#5464=CARTESIAN_POINT ( 'NONE',  ( 30.00000000000000000, 1.102182119232615150E-15, -8.000000000000000000 ) ) ;
#5482=EDGE_CURVE ( 'NONE', #1226, #3851, #4163, .T. ) ;
#5550=EDGE_CURVE ( 'NONE', #1572, #1226, #417, .T. ) ;
#5582=STYLED_ITEM('',(#7624),#6277);
#5586=CARTESIAN_POINT ( 'NONE',  ( 2.000000000000001776, 1.224646799147353651E-15, 10.00000000000000355 ) ) ;
#5587=AXIS2_PLACEMENT_3D ( 'NONE', #1531, #6229, #958 ) ;
#5613=VERTEX_POINT ( 'NONE', #5464 ) ;
#5618=ORIENTED_EDGE ( 'NONE', *, *, #1998, .F. ) ;
#5624=EDGE_CURVE ( 'NONE', #4630, #5613, #5714, .T. ) ;
#5636=CARTESIAN_POINT ( 'NONE',  ( 26.00000000000000000, 7.347880794883831802E-16, -6.000000000000000888 ) ) ;
#5644=ORIENTED_EDGE ( 'NONE', *, *, #962, .T. ) ;
#5653=ORIENTED_EDGE ( 'NONE', *, *, #4853, .F. ) ;
#5682=AXIS2_PLACEMENT_3D ( 'NONE', #6800, #3187, #3152 ) ;
#5694=CYLINDRICAL_SURFACE ( 'NONE', #6937, 10.00000000000000355 ) ;
#5707=AXIS2_PLACEMENT_3D ( 'NONE', #1911, #4841, #6063 ) ;
#5714=CIRCLE ( 'NONE', #1041, 8.000000000000003553 ) ;
#5726=EDGE_LOOP ( 'NONE', ( #4445, #56, #3795, #907 ) ) ;
#5763=ORIENTED_EDGE ( 'NONE', *, *, #2968, .F. ) ;
#5806=DIRECTION ( 'NONE',  ( -1.000000000000000000, -2.624548829666596736E-30, 9.231085635203017994E-31 ) ) ;
#5833=DIRECTION ( 'NONE',  ( -1.000000000000000000, -2.624548829666596736E-30, 9.231085635203017994E-31 ) ) ;
#5853=CARTESIAN_POINT ( 'NONE',  ( 4.000000000000000000, 1.224646799147353651E-15, -10.00000000000000355 ) ) ;
#5884=DIRECTION ( 'NONE',  ( 0.000000000000000000, 0.000000000000000000, -1.000000000000000000 ) ) ;
#5937=ORIENTED_EDGE ( 'NONE', *, *, #5624, .T. ) ;
#5938=PLANE ( 'NONE',  #4889 ) ;
#5956=VECTOR ( 'NONE', #4648, 1000.000000000000114 ) ;
#5958=ORIENTED_EDGE ( 'NONE', *, *, #7567, .T. ) ;
#5963=FACE_OUTER_BOUND ( 'NONE', #218, .T. ) ;
#5975=DIRECTION ( 'NONE',  ( 0.000000000000000000, 0.000000000000000000, -1.000000000000000000 ) ) ;
#5988=EDGE_CURVE ( 'NONE', #6611, #3579, #2008, .T. ) ;
#6013=ORIENTED_EDGE ( 'NONE', *, *, #7097, .F. ) ;
#6063=DIRECTION ( 'NONE',  ( 0.000000000000000000, 0.000000000000000000, -1.000000000000000000 ) ) ;
#6073=DIRECTION ( 'NONE',  ( 0.000000000000000000, 0.000000000000000000, -1.000000000000000000 ) ) ;
#6088=CARTESIAN_POINT ( 'NONE',  ( 26.00000000000000000, 0.000000000000000000, 0.000000000000000000 ) ) ;
#6115=CARTESIAN_POINT ( 'NONE',  ( 4.000000000000000000, 1.224646799147350101E-15, -9.999999999999998224 ) ) ;
#6119=DIRECTION ( 'NONE',  ( -0.7071067811865497932, 8.659560562354715921E-17, -0.7071067811865452413 ) ) ;
#6142=DIRECTION ( 'NONE',  ( 1.000000000000000000, 2.624548829666596736E-30, -9.231085635203017994E-31 ) ) ;
#6167=CARTESIAN_POINT ( 'NONE',  ( 4.000000000000000000, 0.000000000000000000, 0.000000000000000000 ) ) ;
#6171=ORIENTED_EDGE ( 'NONE', *, *, #748, .T. ) ;
#6193=DIRECTION ( 'NONE',  ( 9.231085635203016242E-31, 0.000000000000000000, -1.000000000000000000 ) ) ;
#6196=DIRECTION ( 'NONE',  ( 0.000000000000000000, 0.000000000000000000, 1.000000000000000000 ) ) ;
#6229=DIRECTION ( 'NONE',  ( -1.000000000000000000, -2.624548829666596736E-30, 9.231085635203017994E-31 ) ) ;
#6233=APPLICATION_CONTEXT ( 'automotive_design' ) ;
#6236=CARTESIAN_POINT ( 'NONE',  ( 7.318533788671489235E-30, 1.102182119232615150E-15, 7.999999999999989342 ) ) ;
#6249=DIRECTION ( 'NONE',  ( 1.000000000000000000, 2.624548829666596736E-30, -9.231085635203017994E-31 ) ) ;
#6277=MANIFOLD_SOLID_BREP ( 'Chamfer1', #2090 ) ;
#6286=CONICAL_SURFACE ( 'NONE', #5682, 8.000000000000003553, 0.7853981633974447263 ) ;
#6296=EDGE_LOOP ( 'NONE', ( #3786, #3366, #1191, #5069 ) ) ;
#6303=ADVANCED_FACE ( 'NONE', ( #253 ), #6931, .T. ) ;
#6334=CARTESIAN_POINT ( 'NONE',  ( 4.000000000000000000, -2.624548829666593232E-30, 9.999999999999998224 ) ) ;
#6363=EDGE_CURVE ( 'NONE', #3579, #6611, #4611, .T. ) ;
#6402=CIRCLE ( 'NONE', #2222, 10.00000000000000355 ) ;
#6428=CARTESIAN_POINT ( 'NONE',  ( 4.000000000000000000, 0.000000000000000000, 0.000000000000000000 ) ) ;
#6480=DIRECTION ( 'NONE',  ( 0.000000000000000000, 0.000000000000000000, -1.000000000000000000 ) ) ;
#6486=DIRECTION ( 'NONE',  ( 0.000000000000000000, 0.000000000000000000, -1.000000000000000000 ) ) ;
#6490=CARTESIAN_POINT ( 'NONE',  ( 4.000000000000000000, 7.347880794883831802E-16, -6.000000000000000888 ) ) ;
#6516=PRODUCT_CONTEXT ( 'NONE', #6233, 'mechanical' ) ;
#6519=AXIS2_PLACEMENT_3D ( 'NONE', #6634, #3173, #1357 ) ;
#6522=EDGE_CURVE ( 'NONE', #4660, #959, #2760, .T. ) ;
#6556=CARTESIAN_POINT ( 'NONE',  ( 2.000000000000001776, 0.000000000000000000, 0.000000000000000000 ) ) ;
#6562=FACE_OUTER_BOUND ( 'NONE', #1420, .T. ) ;
#6578=ORIENTED_EDGE ( 'NONE', *, *, #757, .T. ) ;
#6585=EDGE_LOOP ( 'NONE', ( #5653, #765, #1722, #2670 ) ) ;
#6586=EDGE_CURVE ( 'NONE', #5613, #4630, #2396, .T. ) ;
#6596=EDGE_CURVE ( 'NONE', #959, #3851, #1245, .T. ) ;
#6611=VERTEX_POINT ( 'NONE', #4289 ) ;
#6634=CARTESIAN_POINT ( 'NONE',  ( 2.000000000000001776, 0.000000000000000000, 0.000000000000000000 ) ) ;
#6648=AXIS2_PLACEMENT_3D ( 'NONE', #6088, #3277, #811 ) ;
#6674=VECTOR ( 'NONE', #6785, 1000.000000000000000 ) ;
#6690=VECTOR ( 'NONE', #6119, 1000.000000000000227 ) ;
#6708=EDGE_LOOP ( 'NONE', ( #4712, #888, #1558, #3300 ) ) ;
#6713=EDGE_LOOP ( 'NONE', ( #5937, #4572 ) ) ;
#6765=AXIS2_PLACEMENT_3D ( 'NONE', #6556, #1857, #7203 ) ;
#6766=ORIENTED_EDGE ( 'NONE', *, *, #7097, .T. ) ;
#6785=DIRECTION ( 'NONE',  ( -1.000000000000000000, -2.624548829666596736E-30, 9.231085635203017994E-31 ) ) ;
#6795=ADVANCED_FACE ( 'NONE', ( #5088 ), #2087, .T. ) ;
#6800=CARTESIAN_POINT ( 'NONE',  ( 30.00000000000000000, 0.000000000000000000, 0.000000000000000000 ) ) ;
#6807=AXIS2_PLACEMENT_3D ( 'NONE', #454, #7453, #2874 ) ;
#6815=EDGE_LOOP ( 'NONE', ( #7382, #6929, #6824, #2646 ) ) ;
#6824=ORIENTED_EDGE ( 'NONE', *, *, #3893, .T. ) ;
#6841=LINE ( 'NONE', #6991, #6690 ) ;
#6890=CIRCLE ( 'NONE', #2350, 6.000000000000003553 ) ;
#6904=CARTESIAN_POINT ( 'NONE',  ( 4.000000000000000000, 0.000000000000000000, 0.000000000000000000 ) ) ;
#6908=DIRECTION ( 'NONE',  ( 0.000000000000000000, 0.000000000000000000, -1.000000000000000000 ) ) ;
#6924=FACE_OUTER_BOUND ( 'NONE', #6815, .T. ) ;
#6929=ORIENTED_EDGE ( 'NONE', *, *, #5550, .F. ) ;
#6931=CONICAL_SURFACE ( 'NONE', #5707, 10.00000000000000355, 0.7853981633974500554 ) ;
#6937=AXIS2_PLACEMENT_3D ( 'NONE', #6428, #4584, #3354 ) ;
#6991=CARTESIAN_POINT ( 'NONE',  ( 30.00000000000000000, 9.797174393178829602E-16, -8.000000000000003553 ) ) ;
#6996=CARTESIAN_POINT ( 'NONE',  ( 27.99999999999998579, 0.000000000000000000, 0.000000000000000000 ) ) ;
#7020=DIRECTION ( 'NONE',  ( 1.000000000000000000, 2.624548829666596736E-30, -9.231085635203017994E-31 ) ) ;
#7031=ADVANCED_FACE ( 'NONE', ( #4618 ), #5227, .T. ) ;
#7059=LINE ( 'NONE', #4100, #3505 ) ;
#7089=CARTESIAN_POINT ( 'NONE',  ( 2.000000000000001776, 0.000000000000000000, 0.000000000000000000 ) ) ;
#7097=EDGE_CURVE ( 'NONE', #5613, #1936, #6841, .T. ) ;
#7098=CIRCLE ( 'NONE', #1192, 7.999999999999992895 ) ;
#7112=DIRECTION ( 'NONE',  ( 0.000000000000000000, 0.000000000000000000, 1.000000000000000000 ) ) ;
#7173=PLANE ( 'NONE',  #5161 ) ;
#7203=DIRECTION ( 'NONE',  ( 0.000000000000000000, 0.000000000000000000, -1.000000000000000000 ) ) ;
#7213=CARTESIAN_POINT ( 'NONE',  ( 26.00000000000000000, 0.000000000000000000, 0.000000000000000000 ) ) ;
#7257=VERTEX_POINT ( 'NONE', #1296 ) ;
#7359=ORIENTED_EDGE ( 'NONE', *, *, #1938, .T. ) ;
#7382=ORIENTED_EDGE ( 'NONE', *, *, #5482, .F. ) ;
#7389=ORIENTED_EDGE ( 'NONE', *, *, #7567, .F. ) ;
#7402=CARTESIAN_POINT ( 'NONE',  ( 30.00000000000000000, 0.000000000000000000, 0.000000000000000000 ) ) ;
#7418=ORIENTED_EDGE ( 'NONE', *, *, #307, .F. ) ;
#7447=FACE_OUTER_BOUND ( 'NONE', #6713, .T. ) ;
#7453=DIRECTION ( 'NONE',  ( -1.000000000000000000, -2.624548829666596736E-30, 9.231085635203017994E-31 ) ) ;
#7469=DIRECTION ( 'NONE',  ( -1.000000000000000000, -2.624548829666596736E-30, 9.231085635203017994E-31 ) ) ;
#7483=DIRECTION ( 'NONE',  ( 1.000000000000000000, 2.624548829666596736E-30, -9.231085635203017994E-31 ) ) ;
#7500=PRODUCT_DEFINITION_SHAPE ( 'NONE', 'NONE',  #1744 ) ;
#7504=VECTOR ( 'NONE', #2426, 1000.000000000000000 ) ;
#7567=EDGE_CURVE ( 'NONE', #4630, #7257, #7059, .T. ) ;
#7591=DIRECTION ( 'NONE',  ( 9.231085635203016242E-31, 0.000000000000000000, -1.000000000000000000 ) ) ;
#7618=COLOUR_RGB('Light Blue',0.38,0.62,0.78);
#7619=FILL_AREA_STYLE_COLOUR('',#7618);
#7620=FILL_AREA_STYLE('',(#7619));
#7621=SURFACE_STYLE_FILL_AREA(#7620);
#7622=SURFACE_SIDE_STYLE('',(#7621));
#7623=SURFACE_STYLE_USAGE(.BOTH.,#7622);
#7624=PRESENTATION_STYLE_ASSIGNMENT((#7623));
ENDSEC;
END-ISO-10303-21;
